ISO-10303-21;
HEADER;
/* Generated by software containing ST-Developer
 * from STEP Tools, Inc. (www.steptools.com) 
 */

FILE_DESCRIPTION(
/* description */ ('PAT-091'),
/* implementation_level */ '2;1');

FILE_NAME(
/* name */ 'Axle end keeper (9).step',
/* time_stamp */ '2026-10-27T15:34:44-07:00',
/* author */ (''),
/* organization */ (''),
/* preprocessor_version */ 'ST-DEVELOPER v20.2',
/* originating_system */ 'Autodesk Translation Framework v15.17.0.0',
/* authorisation */ '');

FILE_SCHEMA (('AUTOMOTIVE_DESIGN { 1 0 10303 214 3 1 1 }'));
ENDSEC;

DATA;
#10=MECHANICAL_DESIGN_GEOMETRIC_PRESENTATION_REPRESENTATION('',(#1037),#25100);
#817=SHAPE_REPRESENTATION_RELATIONSHIP('SRR','None',#25583,#927);
#927=ADVANCED_BREP_SHAPE_REPRESENTATION('',(#1159),#25053);
#1037=STYLED_ITEM('',(#26191),#1159);
#1159=MANIFOLD_SOLID_BREP('Body1',#13316);
#1512=FACE_BOUND('',#3690,.T.);
#1513=FACE_BOUND('',#3692,.T.);
#1925=PLANE('',#15626);
#1926=PLANE('',#15627);
#2572=FACE_OUTER_BOUND('',#3687,.T.);
#2573=FACE_OUTER_BOUND('',#3688,.T.);
#2574=FACE_OUTER_BOUND('',#3689,.T.);
#2575=FACE_OUTER_BOUND('',#3691,.T.);
#3687=EDGE_LOOP('',(#11008,#11009,#11010,#11011));
#3688=EDGE_LOOP('',(#11012,#11013,#11014,#11015));
#3689=EDGE_LOOP('',(#11016));
#3690=EDGE_LOOP('',(#11017));
#3691=EDGE_LOOP('',(#11018));
#3692=EDGE_LOOP('',(#11019));
#4688=LINE('',#23309,#5428);
#4689=LINE('',#23315,#5429);
#5428=VECTOR('',#19106,0.225000000000001);
#5429=VECTOR('',#19113,1.);
#6054=CIRCLE('',#15621,0.225000000000001);
#6055=CIRCLE('',#15622,0.225000000000001);
#6056=CIRCLE('',#15624,1.);
#6057=CIRCLE('',#15625,1.);
#7059=VERTEX_POINT('',#23306);
#7060=VERTEX_POINT('',#23308);
#7061=VERTEX_POINT('',#23312);
#7062=VERTEX_POINT('',#23314);
#8439=EDGE_CURVE('',#7059,#7059,#6054,.T.);
#8440=EDGE_CURVE('',#7059,#7060,#4688,.T.);
#8441=EDGE_CURVE('',#7060,#7060,#6055,.T.);
#8442=EDGE_CURVE('',#7061,#7061,#6056,.T.);
#8443=EDGE_CURVE('',#7061,#7062,#4689,.T.);
#8444=EDGE_CURVE('',#7062,#7062,#6057,.T.);
#11008=ORIENTED_EDGE('',*,*,#8439,.F.);
#11009=ORIENTED_EDGE('',*,*,#8440,.T.);
#11010=ORIENTED_EDGE('',*,*,#8441,.T.);
#11011=ORIENTED_EDGE('',*,*,#8440,.F.);
#11012=ORIENTED_EDGE('',*,*,#8442,.F.);
#11013=ORIENTED_EDGE('',*,*,#8443,.T.);
#11014=ORIENTED_EDGE('',*,*,#8444,.T.);
#11015=ORIENTED_EDGE('',*,*,#8443,.F.);
#11016=ORIENTED_EDGE('',*,*,#8442,.T.);
#11017=ORIENTED_EDGE('',*,*,#8439,.T.);
#11018=ORIENTED_EDGE('',*,*,#8444,.F.);
#11019=ORIENTED_EDGE('',*,*,#8441,.F.);
#12290=CYLINDRICAL_SURFACE('',#15620,0.225000000000001);
#12291=CYLINDRICAL_SURFACE('',#15623,1.);
#12939=ADVANCED_FACE('',(#2572),#12290,.F.);
#12940=ADVANCED_FACE('',(#2573),#12291,.T.);
#12941=ADVANCED_FACE('',(#2574,#1512),#1925,.T.);
#12942=ADVANCED_FACE('',(#2575,#1513),#1926,.F.);
#13316=CLOSED_SHELL('',(#12939,#12940,#12941,#12942));
#15619=AXIS2_PLACEMENT_3D('',#23304,#19100,#19101);
#15620=AXIS2_PLACEMENT_3D('',#23305,#19102,#19103);
#15621=AXIS2_PLACEMENT_3D('',#23307,#19104,#19105);
#15622=AXIS2_PLACEMENT_3D('',#23310,#19107,#19108);
#15623=AXIS2_PLACEMENT_3D('',#23311,#19109,#19110);
#15624=AXIS2_PLACEMENT_3D('',#23313,#19111,#19112);
#15625=AXIS2_PLACEMENT_3D('',#23316,#19114,#19115);
#15626=AXIS2_PLACEMENT_3D('',#23317,#19116,#19117);
#15627=AXIS2_PLACEMENT_3D('',#23318,#19118,#19119);
#19100=DIRECTION('axis',(0.,0.,1.));
#19101=DIRECTION('refdir',(1.,0.,0.));
#19102=DIRECTION('center_axis',(0.,1.,0.));
#19103=DIRECTION('ref_axis',(1.,0.,0.));
#19104=DIRECTION('center_axis',(0.,-1.,0.));
#19105=DIRECTION('ref_axis',(1.,0.,0.));
#19106=DIRECTION('',(0.,-1.,0.));
#19107=DIRECTION('center_axis',(0.,-1.,0.));
#19108=DIRECTION('ref_axis',(1.,0.,0.));
#19109=DIRECTION('center_axis',(0.,1.,0.));
#19110=DIRECTION('ref_axis',(1.,0.,0.));
#19111=DIRECTION('center_axis',(0.,1.,0.));
#19112=DIRECTION('ref_axis',(1.,0.,0.));
#19113=DIRECTION('',(0.,-1.,0.));
#19114=DIRECTION('center_axis',(0.,1.,0.));
#19115=DIRECTION('ref_axis',(1.,0.,0.));
#19116=DIRECTION('center_axis',(0.,1.,0.));
#19117=DIRECTION('ref_axis',(1.,0.,0.));
#19118=DIRECTION('center_axis',(0.,1.,0.));
#19119=DIRECTION('ref_axis',(1.,0.,0.));
#23304=CARTESIAN_POINT('',(0.,0.,0.));
#23305=CARTESIAN_POINT('Origin',(19.3649167310371,8.5,8.));
#23306=CARTESIAN_POINT('',(19.1399167310371,8.7,8.));
#23307=CARTESIAN_POINT('Origin',(19.3649167310371,8.7,8.));
#23308=CARTESIAN_POINT('',(19.1399167310371,8.5,8.));
#23309=CARTESIAN_POINT('',(19.1399167310371,8.5,8.));
#23310=CARTESIAN_POINT('Origin',(19.3649167310371,8.5,8.));
#23311=CARTESIAN_POINT('Origin',(19.3649167310371,8.5,8.));
#23312=CARTESIAN_POINT('',(18.3649167310371,8.7,8.));
#23313=CARTESIAN_POINT('Origin',(19.3649167310371,8.7,8.));
#23314=CARTESIAN_POINT('',(18.3649167310371,8.5,8.));
#23315=CARTESIAN_POINT('',(18.3649167310371,8.5,8.));
#23316=CARTESIAN_POINT('Origin',(19.3649167310371,8.5,8.));
#23317=CARTESIAN_POINT('Origin',(19.3649167310371,8.7,8.));
#23318=CARTESIAN_POINT('Origin',(19.3649167310371,8.5,8.));
#24932=UNCERTAINTY_MEASURE_WITH_UNIT(LENGTH_MEASURE(0.001),#25101,
'DISTANCE_ACCURACY_VALUE',
'Maximum model space distance between geometric entities at asserted c
onnectivities');
#24979=UNCERTAINTY_MEASURE_WITH_UNIT(LENGTH_MEASURE(0.001),#25101,
'DISTANCE_ACCURACY_VALUE',
'Maximum model space distance between geometric entities at asserted c
onnectivities');
#25053=(
GEOMETRIC_REPRESENTATION_CONTEXT(3)
GLOBAL_UNCERTAINTY_ASSIGNED_CONTEXT((#24932))
GLOBAL_UNIT_ASSIGNED_CONTEXT((#25101,#25103,#25104))
REPRESENTATION_CONTEXT('','3D')
);
#25100=(
GEOMETRIC_REPRESENTATION_CONTEXT(3)
GLOBAL_UNCERTAINTY_ASSIGNED_CONTEXT((#24979))
GLOBAL_UNIT_ASSIGNED_CONTEXT((#25101,#25103,#25104))
REPRESENTATION_CONTEXT('','3D')
);
#25101=(
LENGTH_UNIT()
NAMED_UNIT(*)
SI_UNIT(.CENTI.,.METRE.)
);
#25103=(
NAMED_UNIT(*)
PLANE_ANGLE_UNIT()
SI_UNIT($,.RADIAN.)
);
#25104=(
NAMED_UNIT(*)
SI_UNIT($,.STERADIAN.)
SOLID_ANGLE_UNIT()
);
#25178=SHAPE_DEFINITION_REPRESENTATION(#25300,#25583);
#25300=PRODUCT_DEFINITION_SHAPE('',$,#25704);
#25583=SHAPE_REPRESENTATION('',(#15619),#25053);
#25630=PRODUCT_DEFINITION_CONTEXT('part definition',#25992,'design');
#25704=PRODUCT_DEFINITION('Axle end keeper (9)','Axle end keeper (9)',#25824,
#25630);
#25824=PRODUCT_DEFINITION_FORMATION('',$,#26067);
#25992=APPLICATION_CONTEXT(
'Core Data for Automotive Mechanical Design Process');
#25993=PRODUCT_CONTEXT('part definition',#25992,'mechanical');
#26067=PRODUCT('Axle end keeper (9)','Axle end keeper (9)',
'Axle end keeper (9)',(#25993));
#26185=COLOUR_RGB('Grey',0.48,0.52,0.57);
#26186=FILL_AREA_STYLE_COLOUR('',#26185);
#26187=FILL_AREA_STYLE('',(#26186));
#26188=SURFACE_STYLE_FILL_AREA(#26187);
#26189=SURFACE_SIDE_STYLE('',(#26188));
#26190=SURFACE_STYLE_USAGE(.BOTH.,#26189);
#26191=PRESENTATION_STYLE_ASSIGNMENT((#26190));
ENDSEC;
END-ISO-10303-21;
